ISO-10303-21;
HEADER;
/* Generated by software containing ST-Developer
 * from STEP Tools, Inc. (www.steptools.com) 
 */

FILE_DESCRIPTION(
/* description */ (''),
/* implementation_level */ '2;1');

FILE_NAME(
/* name */ 'Plunger_Pin.step',
/* time_stamp */ '2026-10-23T17:22:31+06:00',
/* author */ (''),
/* organization */ (''),
/* preprocessor_version */ 'ST-DEVELOPER v20.2',
/* originating_system */ 'Autodesk Translation Framework v15.15.0.0',
/* authorisation */ '');

FILE_SCHEMA (('AUTOMOTIVE_DESIGN { 1 0 10303 214 3 1 1 }'));
ENDSEC;

DATA;
#10=MECHANICAL_DESIGN_GEOMETRIC_PRESENTATION_REPRESENTATION('',(#82),#7315);
#51=SPHERICAL_SURFACE('',#3674,1.5);
#62=SHAPE_REPRESENTATION_RELATIONSHIP('SRR','None',#7358,#72);
#72=ADVANCED_BREP_SHAPE_REPRESENTATION('',(#92),#7310);
#82=STYLED_ITEM('',(#7445),#92);
#92=MANIFOLD_SOLID_BREP('Plunger_Pin',#3219);
#382=LINE('',#7232,#542);
#542=VECTOR('',#4575,1.51706056234455);
#683=CYLINDRICAL_SURFACE('',#3683,1.51706056234455);
#696=FACE_BOUND('',#1083,.T.);
#719=PLANE('',#3679);
#720=PLANE('',#3681);
#892=FACE_OUTER_BOUND('',#1081,.T.);
#893=FACE_OUTER_BOUND('',#1082,.T.);
#894=FACE_OUTER_BOUND('',#1084,.T.);
#895=FACE_OUTER_BOUND('',#1085,.T.);
#1081=EDGE_LOOP('',(#2978,#2979,#2980,#2981,#2982,#2983));
#1082=EDGE_LOOP('',(#2984));
#1083=EDGE_LOOP('',(#2985,#2986));
#1084=EDGE_LOOP('',(#2987));
#1085=EDGE_LOOP('',(#2988,#2989,#2990,#2991));
#1271=CIRCLE('',#3675,1.48244108211373);
#1272=CIRCLE('',#3676,1.5);
#1273=CIRCLE('',#3677,1.48244108211373);
#1274=CIRCLE('',#3678,1.5);
#1275=CIRCLE('',#3680,1.51706056234455);
#1276=CIRCLE('',#3682,1.51706056234455);
#1587=VERTEX_POINT('',#7217);
#1588=VERTEX_POINT('',#7218);
#1589=VERTEX_POINT('',#7220);
#1590=VERTEX_POINT('',#7223);
#1591=VERTEX_POINT('',#7226);
#1592=VERTEX_POINT('',#7229);
#2055=EDGE_CURVE('',#1587,#1588,#1271,.T.);
#2056=EDGE_CURVE('',#1587,#1589,#1272,.T.);
#2057=EDGE_CURVE('',#1588,#1587,#1273,.T.);
#2058=EDGE_CURVE('',#1590,#1588,#1274,.T.);
#2059=EDGE_CURVE('',#1591,#1591,#1275,.T.);
#2060=EDGE_CURVE('',#1592,#1592,#1276,.T.);
#2061=EDGE_CURVE('',#1592,#1591,#382,.T.);
#2978=ORIENTED_EDGE('',*,*,#2055,.F.);
#2979=ORIENTED_EDGE('',*,*,#2056,.T.);
#2980=ORIENTED_EDGE('',*,*,#2056,.F.);
#2981=ORIENTED_EDGE('',*,*,#2057,.F.);
#2982=ORIENTED_EDGE('',*,*,#2058,.F.);
#2983=ORIENTED_EDGE('',*,*,#2058,.T.);
#2984=ORIENTED_EDGE('',*,*,#2059,.F.);
#2985=ORIENTED_EDGE('',*,*,#2055,.T.);
#2986=ORIENTED_EDGE('',*,*,#2057,.T.);
#2987=ORIENTED_EDGE('',*,*,#2060,.T.);
#2988=ORIENTED_EDGE('',*,*,#2060,.F.);
#2989=ORIENTED_EDGE('',*,*,#2061,.T.);
#2990=ORIENTED_EDGE('',*,*,#2059,.T.);
#2991=ORIENTED_EDGE('',*,*,#2061,.F.);
#3196=ADVANCED_FACE('',(#892),#51,.F.);
#3197=ADVANCED_FACE('',(#893,#696),#719,.F.);
#3198=ADVANCED_FACE('',(#894),#720,.T.);
#3199=ADVANCED_FACE('',(#895),#683,.T.);
#3219=CLOSED_SHELL('',(#3196,#3197,#3198,#3199));
#3673=AXIS2_PLACEMENT_3D('',#7215,#4553,#4554);
#3674=AXIS2_PLACEMENT_3D('',#7216,#4555,#4556);
#3675=AXIS2_PLACEMENT_3D('',#7219,#4557,#4558);
#3676=AXIS2_PLACEMENT_3D('',#7221,#4559,#4560);
#3677=AXIS2_PLACEMENT_3D('',#7222,#4561,#4562);
#3678=AXIS2_PLACEMENT_3D('',#7224,#4563,#4564);
#3679=AXIS2_PLACEMENT_3D('',#7225,#4565,#4566);
#3680=AXIS2_PLACEMENT_3D('',#7227,#4567,#4568);
#3681=AXIS2_PLACEMENT_3D('',#7228,#4569,#4570);
#3682=AXIS2_PLACEMENT_3D('',#7230,#4571,#4572);
#3683=AXIS2_PLACEMENT_3D('',#7231,#4573,#4574);
#4553=DIRECTION('axis',(0.,0.,1.));
#4554=DIRECTION('refdir',(1.,0.,0.));
#4555=DIRECTION('center_axis',(0.,0.,1.));
#4556=DIRECTION('ref_axis',(1.,0.,0.));
#4557=DIRECTION('center_axis',(1.,0.,0.));
#4558=DIRECTION('ref_axis',(0.,0.,-1.));
#4559=DIRECTION('center_axis',(-1.22464679914735E-16,1.,0.));
#4560=DIRECTION('ref_axis',(-1.,-1.22464679914735E-16,0.));
#4561=DIRECTION('center_axis',(1.,0.,0.));
#4562=DIRECTION('ref_axis',(0.,0.,-1.));
#4563=DIRECTION('center_axis',(-1.22464679914735E-16,1.,0.));
#4564=DIRECTION('ref_axis',(-1.,-1.22464679914735E-16,0.));
#4565=DIRECTION('center_axis',(1.,0.,0.));
#4566=DIRECTION('ref_axis',(0.,0.,-1.));
#4567=DIRECTION('center_axis',(1.,0.,0.));
#4568=DIRECTION('ref_axis',(0.,0.,-1.));
#4569=DIRECTION('center_axis',(1.,0.,0.));
#4570=DIRECTION('ref_axis',(0.,0.,-1.));
#4571=DIRECTION('center_axis',(1.,0.,0.));
#4572=DIRECTION('ref_axis',(0.,0.,-1.));
#4573=DIRECTION('center_axis',(1.,0.,0.));
#4574=DIRECTION('ref_axis',(0.,0.,-1.));
#4575=DIRECTION('',(-1.,0.,0.));
#7215=CARTESIAN_POINT('',(0.,0.,0.));
#7216=CARTESIAN_POINT('Origin',(-9.1,0.,0.));
#7217=CARTESIAN_POINT('',(-9.3288415129767,-1.81546672613512E-16,1.48244108211373));
#7218=CARTESIAN_POINT('',(-9.3288415129767,-2.80250026378947E-17,-1.48244108211373));
#7219=CARTESIAN_POINT('Origin',(-9.3288415129767,0.,0.));
#7220=CARTESIAN_POINT('',(-9.1,-1.12481983699639E-32,1.5));
#7221=CARTESIAN_POINT('Origin',(-9.1,0.,0.));
#7222=CARTESIAN_POINT('Origin',(-9.3288415129767,0.,0.));
#7223=CARTESIAN_POINT('',(-9.1,-1.12481983699639E-32,-1.5));
#7224=CARTESIAN_POINT('Origin',(-9.1,0.,0.));
#7225=CARTESIAN_POINT('Origin',(-9.3288415129767,0.,2.17791759537647));
#7226=CARTESIAN_POINT('',(-9.3288415129767,-1.85786336178794E-16,1.51706056234455));
#7227=CARTESIAN_POINT('Origin',(-9.3288415129767,0.,0.));
#7228=CARTESIAN_POINT('Origin',(-6.41326808244201,0.,0.));
#7229=CARTESIAN_POINT('',(-6.41326808244201,-1.85786336178794E-16,1.51706056234455));
#7230=CARTESIAN_POINT('Origin',(-6.41326808244201,0.,0.));
#7231=CARTESIAN_POINT('Origin',(-8.11443509544501,0.,0.));
#7232=CARTESIAN_POINT('',(-8.11443509544501,-1.85786336178794E-16,1.51706056234455));
#7298=UNCERTAINTY_MEASURE_WITH_UNIT(LENGTH_MEASURE(0.01),#7316,
'DISTANCE_ACCURACY_VALUE',
'Maximum model space distance between geometric entities at asserted c
onnectivities');
#7303=UNCERTAINTY_MEASURE_WITH_UNIT(LENGTH_MEASURE(0.01),#7316,
'DISTANCE_ACCURACY_VALUE',
'Maximum model space distance between geometric entities at asserted c
onnectivities');
#7310=(
GEOMETRIC_REPRESENTATION_CONTEXT(3)
GLOBAL_UNCERTAINTY_ASSIGNED_CONTEXT((#7298))
GLOBAL_UNIT_ASSIGNED_CONTEXT((#7316,#7318,#7319))
REPRESENTATION_CONTEXT('','3D')
);
#7315=(
GEOMETRIC_REPRESENTATION_CONTEXT(3)
GLOBAL_UNCERTAINTY_ASSIGNED_CONTEXT((#7303))
GLOBAL_UNIT_ASSIGNED_CONTEXT((#7316,#7318,#7319))
REPRESENTATION_CONTEXT('','3D')
);
#7316=(
LENGTH_UNIT()
NAMED_UNIT(*)
SI_UNIT(.MILLI.,.METRE.)
);
#7318=(
NAMED_UNIT(*)
PLANE_ANGLE_UNIT()
SI_UNIT($,.RADIAN.)
);
#7319=(
NAMED_UNIT(*)
SI_UNIT($,.STERADIAN.)
SOLID_ANGLE_UNIT()
);
#7326=SHAPE_DEFINITION_REPRESENTATION(#7337,#7358);
#7337=PRODUCT_DEFINITION_SHAPE('',$,#7370);
#7358=SHAPE_REPRESENTATION('',(#3673),#7310);
#7363=PRODUCT_DEFINITION_CONTEXT('part definition',#7398,'design');
#7370=PRODUCT_DEFINITION('Plunger_Pin','Plunger_Pin',#7381,#7363);
#7381=PRODUCT_DEFINITION_FORMATION('',$,#7406);
#7398=APPLICATION_CONTEXT(
'Core Data for Automotive Mechanical Design Process');
#7399=PRODUCT_CONTEXT('part definition',#7398,'mechanical');
#7406=PRODUCT('Plunger_Pin','Plunger_Pin',$,(#7399));
#7439=COLOUR_RGB('Grey',0.48,0.52,0.57);
#7440=FILL_AREA_STYLE_COLOUR('',#7439);
#7441=FILL_AREA_STYLE('',(#7440));
#7442=SURFACE_STYLE_FILL_AREA(#7441);
#7443=SURFACE_SIDE_STYLE('',(#7442));
#7444=SURFACE_STYLE_USAGE(.BOTH.,#7443);
#7445=PRESENTATION_STYLE_ASSIGNMENT((#7444));
ENDSEC;
END-ISO-10303-21;
